ISO-10303-21;
HEADER;
/* Generated by software containing ST-Developer
 * from STEP Tools, Inc. (www.steptools.com) 
 */

FILE_DESCRIPTION(
/* description */ ('Cam-and-follower valve demonstrator'),
/* implementation_level */ '2;1');

FILE_NAME(
/* name */ 'Camshaft bearing post (1).step',
/* time_stamp */ '2026-10-28T03:25:17-07:00',
/* author */ (''),
/* organization */ (''),
/* preprocessor_version */ 'ST-DEVELOPER v20.2',
/* originating_system */ 'Autodesk Translation Framework v15.17.0.0',
/* authorisation */ '');

FILE_SCHEMA (('AUTOMOTIVE_DESIGN { 1 0 10303 214 3 1 1 }'));
ENDSEC;

DATA;
#10=MECHANICAL_DESIGN_GEOMETRIC_PRESENTATION_REPRESENTATION('',(#418),#12896);
#346=SHAPE_REPRESENTATION_RELATIONSHIP('SRR','None',#13062,#382);
#382=ADVANCED_BREP_SHAPE_REPRESENTATION('',(#461),#12862);
#418=STYLED_ITEM('',(#13330),#461);
#461=MANIFOLD_SOLID_BREP('Body1',#6185);
#544=FACE_BOUND('',#1586,.T.);
#545=FACE_BOUND('',#1588,.T.);
#546=FACE_BOUND('',#1592,.T.);
#547=FACE_BOUND('',#1593,.T.);
#548=FACE_BOUND('',#1594,.T.);
#549=FACE_BOUND('',#1595,.T.);
#550=FACE_BOUND('',#1596,.T.);
#551=FACE_BOUND('',#1599,.T.);
#552=FACE_BOUND('',#1600,.T.);
#553=FACE_BOUND('',#1601,.T.);
#554=FACE_BOUND('',#1602,.T.);
#555=FACE_BOUND('',#1603,.T.);
#556=FACE_BOUND('',#1607,.T.);
#557=FACE_BOUND('',#1608,.T.);
#713=CIRCLE('',#6752,0.225);
#714=CIRCLE('',#6753,0.225);
#715=CIRCLE('',#6755,0.225);
#716=CIRCLE('',#6756,0.225);
#717=CIRCLE('',#6758,0.165);
#718=CIRCLE('',#6759,0.165);
#719=CIRCLE('',#6761,0.165);
#720=CIRCLE('',#6762,0.165);
#721=CIRCLE('',#6764,0.165);
#722=CIRCLE('',#6765,0.165);
#723=CIRCLE('',#6767,0.165);
#724=CIRCLE('',#6768,0.165);
#725=CIRCLE('',#6770,1.6);
#726=CIRCLE('',#6771,1.6);
#1000=CYLINDRICAL_SURFACE('',#6751,0.225);
#1001=CYLINDRICAL_SURFACE('',#6754,0.225);
#1002=CYLINDRICAL_SURFACE('',#6757,0.165);
#1003=CYLINDRICAL_SURFACE('',#6760,0.165);
#1004=CYLINDRICAL_SURFACE('',#6763,0.165);
#1005=CYLINDRICAL_SURFACE('',#6766,0.165);
#1006=CYLINDRICAL_SURFACE('',#6769,1.6);
#1161=FACE_OUTER_BOUND('',#1578,.T.);
#1162=FACE_OUTER_BOUND('',#1579,.T.);
#1163=FACE_OUTER_BOUND('',#1580,.T.);
#1164=FACE_OUTER_BOUND('',#1581,.T.);
#1165=FACE_OUTER_BOUND('',#1582,.T.);
#1166=FACE_OUTER_BOUND('',#1583,.T.);
#1167=FACE_OUTER_BOUND('',#1584,.T.);
#1168=FACE_OUTER_BOUND('',#1585,.T.);
#1169=FACE_OUTER_BOUND('',#1587,.T.);
#1170=FACE_OUTER_BOUND('',#1589,.T.);
#1171=FACE_OUTER_BOUND('',#1590,.T.);
#1172=FACE_OUTER_BOUND('',#1591,.T.);
#1173=FACE_OUTER_BOUND('',#1597,.T.);
#1174=FACE_OUTER_BOUND('',#1598,.T.);
#1175=FACE_OUTER_BOUND('',#1604,.T.);
#1176=FACE_OUTER_BOUND('',#1605,.T.);
#1177=FACE_OUTER_BOUND('',#1606,.T.);
#1578=EDGE_LOOP('',(#4401,#4402,#4403,#4404));
#1579=EDGE_LOOP('',(#4405,#4406,#4407,#4408));
#1580=EDGE_LOOP('',(#4409,#4410,#4411,#4412));
#1581=EDGE_LOOP('',(#4413,#4414,#4415,#4416));
#1582=EDGE_LOOP('',(#4417,#4418,#4419,#4420));
#1583=EDGE_LOOP('',(#4421,#4422,#4423,#4424));
#1584=EDGE_LOOP('',(#4425,#4426,#4427,#4428));
#1585=EDGE_LOOP('',(#4429,#4430,#4431,#4432));
#1586=EDGE_LOOP('',(#4433));
#1587=EDGE_LOOP('',(#4434,#4435,#4436,#4437));
#1588=EDGE_LOOP('',(#4438));
#1589=EDGE_LOOP('',(#4439,#4440,#4441,#4442));
#1590=EDGE_LOOP('',(#4443,#4444,#4445,#4446));
#1591=EDGE_LOOP('',(#4447,#4448,#4449,#4450,#4451,#4452,#4453,#4454));
#1592=EDGE_LOOP('',(#4455));
#1593=EDGE_LOOP('',(#4456));
#1594=EDGE_LOOP('',(#4457));
#1595=EDGE_LOOP('',(#4458));
#1596=EDGE_LOOP('',(#4459));
#1597=EDGE_LOOP('',(#4460,#4461,#4462,#4463));
#1598=EDGE_LOOP('',(#4464,#4465,#4466,#4467,#4468,#4469,#4470,#4471));
#1599=EDGE_LOOP('',(#4472));
#1600=EDGE_LOOP('',(#4473));
#1601=EDGE_LOOP('',(#4474));
#1602=EDGE_LOOP('',(#4475));
#1603=EDGE_LOOP('',(#4476));
#1604=EDGE_LOOP('',(#4477,#4478,#4479,#4480));
#1605=EDGE_LOOP('',(#4481,#4482,#4483,#4484));
#1606=EDGE_LOOP('',(#4485,#4486,#4487,#4488));
#1607=EDGE_LOOP('',(#4489));
#1608=EDGE_LOOP('',(#4490));
#2094=LINE('',#9754,#2516);
#2095=LINE('',#9760,#2517);
#2096=LINE('',#9766,#2518);
#2097=LINE('',#9772,#2519);
#2098=LINE('',#9778,#2520);
#2099=LINE('',#9784,#2521);
#2100=LINE('',#9790,#2522);
#2101=LINE('',#9795,#2523);
#2102=LINE('',#9797,#2524);
#2103=LINE('',#9799,#2525);
#2104=LINE('',#9800,#2526);
#2105=LINE('',#9804,#2527);
#2106=LINE('',#9806,#2528);
#2107=LINE('',#9808,#2529);
#2108=LINE('',#9809,#2530);
#2109=LINE('',#9812,#2531);
#2110=LINE('',#9814,#2532);
#2111=LINE('',#9815,#2533);
#2112=LINE('',#9818,#2534);
#2113=LINE('',#9820,#2535);
#2114=LINE('',#9821,#2536);
#2115=LINE('',#9824,#2537);
#2116=LINE('',#9826,#2538);
#2117=LINE('',#9827,#2539);
#2118=LINE('',#9828,#2540);
#2119=LINE('',#9831,#2541);
#2120=LINE('',#9832,#2542);
#2121=LINE('',#9835,#2543);
#2122=LINE('',#9836,#2544);
#2123=LINE('',#9837,#2545);
#2124=LINE('',#9839,#2546);
#2516=VECTOR('',#7775,0.225);
#2517=VECTOR('',#7782,0.225);
#2518=VECTOR('',#7789,0.165);
#2519=VECTOR('',#7796,0.165);
#2520=VECTOR('',#7803,0.165);
#2521=VECTOR('',#7810,0.165);
#2522=VECTOR('',#7817,1.6);
#2523=VECTOR('',#7822,1.);
#2524=VECTOR('',#7823,1.);
#2525=VECTOR('',#7824,1.);
#2526=VECTOR('',#7825,1.);
#2527=VECTOR('',#7828,1.);
#2528=VECTOR('',#7829,1.);
#2529=VECTOR('',#7830,1.);
#2530=VECTOR('',#7831,1.);
#2531=VECTOR('',#7834,1.);
#2532=VECTOR('',#7835,1.);
#2533=VECTOR('',#7836,1.);
#2534=VECTOR('',#7839,1.);
#2535=VECTOR('',#7840,1.);
#2536=VECTOR('',#7841,1.);
#2537=VECTOR('',#7844,1.);
#2538=VECTOR('',#7845,1.);
#2539=VECTOR('',#7846,1.);
#2540=VECTOR('',#7847,1.);
#2541=VECTOR('',#7850,1.);
#2542=VECTOR('',#7851,1.);
#2543=VECTOR('',#7854,1.);
#2544=VECTOR('',#7855,1.);
#2545=VECTOR('',#7856,1.);
#2546=VECTOR('',#7859,1.);
#2941=VERTEX_POINT('',#9751);
#2942=VERTEX_POINT('',#9753);
#2943=VERTEX_POINT('',#9757);
#2944=VERTEX_POINT('',#9759);
#2945=VERTEX_POINT('',#9763);
#2946=VERTEX_POINT('',#9765);
#2947=VERTEX_POINT('',#9769);
#2948=VERTEX_POINT('',#9771);
#2949=VERTEX_POINT('',#9775);
#2950=VERTEX_POINT('',#9777);
#2951=VERTEX_POINT('',#9781);
#2952=VERTEX_POINT('',#9783);
#2953=VERTEX_POINT('',#9787);
#2954=VERTEX_POINT('',#9789);
#2955=VERTEX_POINT('',#9793);
#2956=VERTEX_POINT('',#9794);
#2957=VERTEX_POINT('',#9796);
#2958=VERTEX_POINT('',#9798);
#2959=VERTEX_POINT('',#9802);
#2960=VERTEX_POINT('',#9803);
#2961=VERTEX_POINT('',#9805);
#2962=VERTEX_POINT('',#9807);
#2963=VERTEX_POINT('',#9811);
#2964=VERTEX_POINT('',#9813);
#2965=VERTEX_POINT('',#9817);
#2966=VERTEX_POINT('',#9819);
#2967=VERTEX_POINT('',#9823);
#2968=VERTEX_POINT('',#9825);
#2969=VERTEX_POINT('',#9830);
#2970=VERTEX_POINT('',#9834);
#3497=EDGE_CURVE('',#2941,#2941,#713,.T.);
#3498=EDGE_CURVE('',#2941,#2942,#2094,.T.);
#3499=EDGE_CURVE('',#2942,#2942,#714,.T.);
#3500=EDGE_CURVE('',#2943,#2943,#715,.T.);
#3501=EDGE_CURVE('',#2943,#2944,#2095,.T.);
#3502=EDGE_CURVE('',#2944,#2944,#716,.T.);
#3503=EDGE_CURVE('',#2945,#2945,#717,.T.);
#3504=EDGE_CURVE('',#2945,#2946,#2096,.T.);
#3505=EDGE_CURVE('',#2946,#2946,#718,.T.);
#3506=EDGE_CURVE('',#2947,#2947,#719,.T.);
#3507=EDGE_CURVE('',#2947,#2948,#2097,.T.);
#3508=EDGE_CURVE('',#2948,#2948,#720,.T.);
#3509=EDGE_CURVE('',#2949,#2949,#721,.T.);
#3510=EDGE_CURVE('',#2949,#2950,#2098,.T.);
#3511=EDGE_CURVE('',#2950,#2950,#722,.T.);
#3512=EDGE_CURVE('',#2951,#2951,#723,.T.);
#3513=EDGE_CURVE('',#2951,#2952,#2099,.T.);
#3514=EDGE_CURVE('',#2952,#2952,#724,.T.);
#3515=EDGE_CURVE('',#2953,#2953,#725,.T.);
#3516=EDGE_CURVE('',#2953,#2954,#2100,.T.);
#3517=EDGE_CURVE('',#2954,#2954,#726,.T.);
#3518=EDGE_CURVE('',#2955,#2956,#2101,.T.);
#3519=EDGE_CURVE('',#2957,#2955,#2102,.T.);
#3520=EDGE_CURVE('',#2957,#2958,#2103,.T.);
#3521=EDGE_CURVE('',#2956,#2958,#2104,.T.);
#3522=EDGE_CURVE('',#2959,#2960,#2105,.T.);
#3523=EDGE_CURVE('',#2961,#2959,#2106,.T.);
#3524=EDGE_CURVE('',#2962,#2961,#2107,.T.);
#3525=EDGE_CURVE('',#2960,#2962,#2108,.T.);
#3526=EDGE_CURVE('',#2962,#2963,#2109,.T.);
#3527=EDGE_CURVE('',#2964,#2961,#2110,.T.);
#3528=EDGE_CURVE('',#2963,#2964,#2111,.T.);
#3529=EDGE_CURVE('',#2965,#2957,#2112,.T.);
#3530=EDGE_CURVE('',#2965,#2966,#2113,.T.);
#3531=EDGE_CURVE('',#2958,#2966,#2114,.T.);
#3532=EDGE_CURVE('',#2955,#2967,#2115,.T.);
#3533=EDGE_CURVE('',#2968,#2967,#2116,.T.);
#3534=EDGE_CURVE('',#2960,#2968,#2117,.T.);
#3535=EDGE_CURVE('',#2963,#2965,#2118,.T.);
#3536=EDGE_CURVE('',#2956,#2969,#2119,.T.);
#3537=EDGE_CURVE('',#2967,#2969,#2120,.T.);
#3538=EDGE_CURVE('',#2959,#2970,#2121,.T.);
#3539=EDGE_CURVE('',#2969,#2970,#2122,.T.);
#3540=EDGE_CURVE('',#2966,#2964,#2123,.T.);
#3541=EDGE_CURVE('',#2970,#2968,#2124,.T.);
#4401=ORIENTED_EDGE('',*,*,#3497,.F.);
#4402=ORIENTED_EDGE('',*,*,#3498,.T.);
#4403=ORIENTED_EDGE('',*,*,#3499,.F.);
#4404=ORIENTED_EDGE('',*,*,#3498,.F.);
#4405=ORIENTED_EDGE('',*,*,#3500,.F.);
#4406=ORIENTED_EDGE('',*,*,#3501,.T.);
#4407=ORIENTED_EDGE('',*,*,#3502,.F.);
#4408=ORIENTED_EDGE('',*,*,#3501,.F.);
#4409=ORIENTED_EDGE('',*,*,#3503,.F.);
#4410=ORIENTED_EDGE('',*,*,#3504,.T.);
#4411=ORIENTED_EDGE('',*,*,#3505,.F.);
#4412=ORIENTED_EDGE('',*,*,#3504,.F.);
#4413=ORIENTED_EDGE('',*,*,#3506,.F.);
#4414=ORIENTED_EDGE('',*,*,#3507,.T.);
#4415=ORIENTED_EDGE('',*,*,#3508,.F.);
#4416=ORIENTED_EDGE('',*,*,#3507,.F.);
#4417=ORIENTED_EDGE('',*,*,#3509,.F.);
#4418=ORIENTED_EDGE('',*,*,#3510,.T.);
#4419=ORIENTED_EDGE('',*,*,#3511,.F.);
#4420=ORIENTED_EDGE('',*,*,#3510,.F.);
#4421=ORIENTED_EDGE('',*,*,#3512,.F.);
#4422=ORIENTED_EDGE('',*,*,#3513,.T.);
#4423=ORIENTED_EDGE('',*,*,#3514,.F.);
#4424=ORIENTED_EDGE('',*,*,#3513,.F.);
#4425=ORIENTED_EDGE('',*,*,#3515,.F.);
#4426=ORIENTED_EDGE('',*,*,#3516,.T.);
#4427=ORIENTED_EDGE('',*,*,#3517,.F.);
#4428=ORIENTED_EDGE('',*,*,#3516,.F.);
#4429=ORIENTED_EDGE('',*,*,#3518,.F.);
#4430=ORIENTED_EDGE('',*,*,#3519,.F.);
#4431=ORIENTED_EDGE('',*,*,#3520,.T.);
#4432=ORIENTED_EDGE('',*,*,#3521,.F.);
#4433=ORIENTED_EDGE('',*,*,#3502,.T.);
#4434=ORIENTED_EDGE('',*,*,#3522,.F.);
#4435=ORIENTED_EDGE('',*,*,#3523,.F.);
#4436=ORIENTED_EDGE('',*,*,#3524,.F.);
#4437=ORIENTED_EDGE('',*,*,#3525,.F.);
#4438=ORIENTED_EDGE('',*,*,#3499,.T.);
#4439=ORIENTED_EDGE('',*,*,#3526,.F.);
#4440=ORIENTED_EDGE('',*,*,#3524,.T.);
#4441=ORIENTED_EDGE('',*,*,#3527,.F.);
#4442=ORIENTED_EDGE('',*,*,#3528,.F.);
#4443=ORIENTED_EDGE('',*,*,#3529,.F.);
#4444=ORIENTED_EDGE('',*,*,#3530,.T.);
#4445=ORIENTED_EDGE('',*,*,#3531,.F.);
#4446=ORIENTED_EDGE('',*,*,#3520,.F.);
#4447=ORIENTED_EDGE('',*,*,#3532,.T.);
#4448=ORIENTED_EDGE('',*,*,#3533,.F.);
#4449=ORIENTED_EDGE('',*,*,#3534,.F.);
#4450=ORIENTED_EDGE('',*,*,#3525,.T.);
#4451=ORIENTED_EDGE('',*,*,#3526,.T.);
#4452=ORIENTED_EDGE('',*,*,#3535,.T.);
#4453=ORIENTED_EDGE('',*,*,#3529,.T.);
#4454=ORIENTED_EDGE('',*,*,#3519,.T.);
#4455=ORIENTED_EDGE('',*,*,#3515,.T.);
#4456=ORIENTED_EDGE('',*,*,#3512,.T.);
#4457=ORIENTED_EDGE('',*,*,#3509,.T.);
#4458=ORIENTED_EDGE('',*,*,#3506,.T.);
#4459=ORIENTED_EDGE('',*,*,#3503,.T.);
#4460=ORIENTED_EDGE('',*,*,#3518,.T.);
#4461=ORIENTED_EDGE('',*,*,#3536,.T.);
#4462=ORIENTED_EDGE('',*,*,#3537,.F.);
#4463=ORIENTED_EDGE('',*,*,#3532,.F.);
#4464=ORIENTED_EDGE('',*,*,#3538,.T.);
#4465=ORIENTED_EDGE('',*,*,#3539,.F.);
#4466=ORIENTED_EDGE('',*,*,#3536,.F.);
#4467=ORIENTED_EDGE('',*,*,#3521,.T.);
#4468=ORIENTED_EDGE('',*,*,#3531,.T.);
#4469=ORIENTED_EDGE('',*,*,#3540,.T.);
#4470=ORIENTED_EDGE('',*,*,#3527,.T.);
#4471=ORIENTED_EDGE('',*,*,#3523,.T.);
#4472=ORIENTED_EDGE('',*,*,#3517,.T.);
#4473=ORIENTED_EDGE('',*,*,#3514,.T.);
#4474=ORIENTED_EDGE('',*,*,#3511,.T.);
#4475=ORIENTED_EDGE('',*,*,#3508,.T.);
#4476=ORIENTED_EDGE('',*,*,#3505,.T.);
#4477=ORIENTED_EDGE('',*,*,#3522,.T.);
#4478=ORIENTED_EDGE('',*,*,#3534,.T.);
#4479=ORIENTED_EDGE('',*,*,#3541,.F.);
#4480=ORIENTED_EDGE('',*,*,#3538,.F.);
#4481=ORIENTED_EDGE('',*,*,#3541,.T.);
#4482=ORIENTED_EDGE('',*,*,#3533,.T.);
#4483=ORIENTED_EDGE('',*,*,#3537,.T.);
#4484=ORIENTED_EDGE('',*,*,#3539,.T.);
#4485=ORIENTED_EDGE('',*,*,#3540,.F.);
#4486=ORIENTED_EDGE('',*,*,#3530,.F.);
#4487=ORIENTED_EDGE('',*,*,#3535,.F.);
#4488=ORIENTED_EDGE('',*,*,#3528,.T.);
#4489=ORIENTED_EDGE('',*,*,#3497,.T.);
#4490=ORIENTED_EDGE('',*,*,#3500,.T.);
#5636=PLANE('',#6772);
#5637=PLANE('',#6773);
#5638=PLANE('',#6774);
#5639=PLANE('',#6775);
#5640=PLANE('',#6776);
#5641=PLANE('',#6777);
#5642=PLANE('',#6778);
#5643=PLANE('',#6779);
#5644=PLANE('',#6780);
#5645=PLANE('',#6781);
#5877=ADVANCED_FACE('',(#1161),#1000,.F.);
#5878=ADVANCED_FACE('',(#1162),#1001,.F.);
#5879=ADVANCED_FACE('',(#1163),#1002,.F.);
#5880=ADVANCED_FACE('',(#1164),#1003,.F.);
#5881=ADVANCED_FACE('',(#1165),#1004,.F.);
#5882=ADVANCED_FACE('',(#1166),#1005,.F.);
#5883=ADVANCED_FACE('',(#1167),#1006,.F.);
#5884=ADVANCED_FACE('',(#1168,#544),#5636,.T.);
#5885=ADVANCED_FACE('',(#1169,#545),#5637,.T.);
#5886=ADVANCED_FACE('',(#1170),#5638,.T.);
#5887=ADVANCED_FACE('',(#1171),#5639,.T.);
#5888=ADVANCED_FACE('',(#1172,#546,#547,#548,#549,#550),#5640,.T.);
#5889=ADVANCED_FACE('',(#1173),#5641,.T.);
#5890=ADVANCED_FACE('',(#1174,#551,#552,#553,#554,#555),#5642,.T.);
#5891=ADVANCED_FACE('',(#1175),#5643,.T.);
#5892=ADVANCED_FACE('',(#1176),#5644,.T.);
#5893=ADVANCED_FACE('',(#1177,#556,#557),#5645,.F.);
#6185=CLOSED_SHELL('',(#5877,#5878,#5879,#5880,#5881,#5882,#5883,#5884,
#5885,#5886,#5887,#5888,#5889,#5890,#5891,#5892,#5893));
#6750=AXIS2_PLACEMENT_3D('',#9749,#7769,#7770);
#6751=AXIS2_PLACEMENT_3D('',#9750,#7771,#7772);
#6752=AXIS2_PLACEMENT_3D('',#9752,#7773,#7774);
#6753=AXIS2_PLACEMENT_3D('',#9755,#7776,#7777);
#6754=AXIS2_PLACEMENT_3D('',#9756,#7778,#7779);
#6755=AXIS2_PLACEMENT_3D('',#9758,#7780,#7781);
#6756=AXIS2_PLACEMENT_3D('',#9761,#7783,#7784);
#6757=AXIS2_PLACEMENT_3D('',#9762,#7785,#7786);
#6758=AXIS2_PLACEMENT_3D('',#9764,#7787,#7788);
#6759=AXIS2_PLACEMENT_3D('',#9767,#7790,#7791);
#6760=AXIS2_PLACEMENT_3D('',#9768,#7792,#7793);
#6761=AXIS2_PLACEMENT_3D('',#9770,#7794,#7795);
#6762=AXIS2_PLACEMENT_3D('',#9773,#7797,#7798);
#6763=AXIS2_PLACEMENT_3D('',#9774,#7799,#7800);
#6764=AXIS2_PLACEMENT_3D('',#9776,#7801,#7802);
#6765=AXIS2_PLACEMENT_3D('',#9779,#7804,#7805);
#6766=AXIS2_PLACEMENT_3D('',#9780,#7806,#7807);
#6767=AXIS2_PLACEMENT_3D('',#9782,#7808,#7809);
#6768=AXIS2_PLACEMENT_3D('',#9785,#7811,#7812);
#6769=AXIS2_PLACEMENT_3D('',#9786,#7813,#7814);
#6770=AXIS2_PLACEMENT_3D('',#9788,#7815,#7816);
#6771=AXIS2_PLACEMENT_3D('',#9791,#7818,#7819);
#6772=AXIS2_PLACEMENT_3D('',#9792,#7820,#7821);
#6773=AXIS2_PLACEMENT_3D('',#9801,#7826,#7827);
#6774=AXIS2_PLACEMENT_3D('',#9810,#7832,#7833);
#6775=AXIS2_PLACEMENT_3D('',#9816,#7837,#7838);
#6776=AXIS2_PLACEMENT_3D('',#9822,#7842,#7843);
#6777=AXIS2_PLACEMENT_3D('',#9829,#7848,#7849);
#6778=AXIS2_PLACEMENT_3D('',#9833,#7852,#7853);
#6779=AXIS2_PLACEMENT_3D('',#9838,#7857,#7858);
#6780=AXIS2_PLACEMENT_3D('',#9840,#7860,#7861);
#6781=AXIS2_PLACEMENT_3D('',#9841,#7862,#7863);
#7769=DIRECTION('axis',(0.,0.,1.));
#7770=DIRECTION('refdir',(1.,0.,0.));
#7771=DIRECTION('center_axis',(0.,0.,1.));
#7772=DIRECTION('ref_axis',(1.,0.,0.));
#7773=DIRECTION('center_axis',(0.,0.,1.));
#7774=DIRECTION('ref_axis',(1.,0.,0.));
#7775=DIRECTION('',(0.,0.,1.));
#7776=DIRECTION('center_axis',(0.,0.,-1.));
#7777=DIRECTION('ref_axis',(1.,0.,0.));
#7778=DIRECTION('center_axis',(0.,0.,1.));
#7779=DIRECTION('ref_axis',(1.,0.,0.));
#7780=DIRECTION('center_axis',(0.,0.,1.));
#7781=DIRECTION('ref_axis',(1.,0.,0.));
#7782=DIRECTION('',(0.,0.,1.));
#7783=DIRECTION('center_axis',(0.,0.,-1.));
#7784=DIRECTION('ref_axis',(1.,0.,0.));
#7785=DIRECTION('center_axis',(0.,1.,0.));
#7786=DIRECTION('ref_axis',(1.,0.,0.));
#7787=DIRECTION('center_axis',(0.,1.,0.));
#7788=DIRECTION('ref_axis',(1.,0.,0.));
#7789=DIRECTION('',(0.,1.,0.));
#7790=DIRECTION('center_axis',(0.,-1.,0.));
#7791=DIRECTION('ref_axis',(1.,0.,0.));
#7792=DIRECTION('center_axis',(0.,1.,0.));
#7793=DIRECTION('ref_axis',(1.,0.,0.));
#7794=DIRECTION('center_axis',(0.,1.,0.));
#7795=DIRECTION('ref_axis',(1.,0.,0.));
#7796=DIRECTION('',(0.,1.,0.));
#7797=DIRECTION('center_axis',(0.,-1.,0.));
#7798=DIRECTION('ref_axis',(1.,0.,0.));
#7799=DIRECTION('center_axis',(0.,1.,0.));
#7800=DIRECTION('ref_axis',(1.,0.,0.));
#7801=DIRECTION('center_axis',(0.,1.,0.));
#7802=DIRECTION('ref_axis',(1.,0.,0.));
#7803=DIRECTION('',(0.,1.,0.));
#7804=DIRECTION('center_axis',(0.,-1.,0.));
#7805=DIRECTION('ref_axis',(1.,0.,0.));
#7806=DIRECTION('center_axis',(0.,1.,0.));
#7807=DIRECTION('ref_axis',(1.,0.,0.));
#7808=DIRECTION('center_axis',(0.,1.,0.));
#7809=DIRECTION('ref_axis',(1.,0.,0.));
#7810=DIRECTION('',(0.,1.,0.));
#7811=DIRECTION('center_axis',(0.,-1.,0.));
#7812=DIRECTION('ref_axis',(1.,0.,0.));
#7813=DIRECTION('center_axis',(0.,1.,0.));
#7814=DIRECTION('ref_axis',(1.,0.,0.));
#7815=DIRECTION('center_axis',(0.,1.,0.));
#7816=DIRECTION('ref_axis',(1.,0.,0.));
#7817=DIRECTION('',(0.,1.,0.));
#7818=DIRECTION('center_axis',(0.,-1.,0.));
#7819=DIRECTION('ref_axis',(1.,0.,0.));
#7820=DIRECTION('center_axis',(0.,0.,1.));
#7821=DIRECTION('ref_axis',(1.,0.,0.));
#7822=DIRECTION('',(0.,1.,0.));
#7823=DIRECTION('',(-1.,0.,0.));
#7824=DIRECTION('',(0.,1.,0.));
#7825=DIRECTION('',(1.,0.,0.));
#7826=DIRECTION('center_axis',(0.,0.,1.));
#7827=DIRECTION('ref_axis',(1.,0.,0.));
#7828=DIRECTION('',(0.,-1.,0.));
#7829=DIRECTION('',(1.,0.,0.));
#7830=DIRECTION('',(0.,1.,0.));
#7831=DIRECTION('',(-1.,0.,0.));
#7832=DIRECTION('center_axis',(-1.,0.,0.));
#7833=DIRECTION('ref_axis',(0.,0.,1.));
#7834=DIRECTION('',(0.,0.,-1.));
#7835=DIRECTION('',(0.,0.,1.));
#7836=DIRECTION('',(0.,1.,0.));
#7837=DIRECTION('center_axis',(1.,0.,0.));
#7838=DIRECTION('ref_axis',(0.,0.,-1.));
#7839=DIRECTION('',(0.,0.,1.));
#7840=DIRECTION('',(0.,1.,0.));
#7841=DIRECTION('',(0.,0.,-1.));
#7842=DIRECTION('center_axis',(0.,-1.,0.));
#7843=DIRECTION('ref_axis',(1.,0.,0.));
#7844=DIRECTION('',(0.,0.,1.));
#7845=DIRECTION('',(1.,0.,0.));
#7846=DIRECTION('',(0.,0.,1.));
#7847=DIRECTION('',(1.,0.,0.));
#7848=DIRECTION('center_axis',(1.,0.,0.));
#7849=DIRECTION('ref_axis',(0.,1.,0.));
#7850=DIRECTION('',(0.,0.,1.));
#7851=DIRECTION('',(0.,1.,0.));
#7852=DIRECTION('center_axis',(0.,1.,0.));
#7853=DIRECTION('ref_axis',(-1.,0.,0.));
#7854=DIRECTION('',(0.,0.,1.));
#7855=DIRECTION('',(-1.,0.,0.));
#7856=DIRECTION('',(-1.,0.,0.));
#7857=DIRECTION('center_axis',(-1.,0.,0.));
#7858=DIRECTION('ref_axis',(0.,-1.,0.));
#7859=DIRECTION('',(0.,-1.,0.));
#7860=DIRECTION('center_axis',(0.,0.,1.));
#7861=DIRECTION('ref_axis',(1.,0.,0.));
#7862=DIRECTION('center_axis',(0.,0.,1.));
#7863=DIRECTION('ref_axis',(1.,0.,0.));
#9749=CARTESIAN_POINT('',(0.,0.,0.));
#9750=CARTESIAN_POINT('Origin',(-3.,2.5,0.9));
#9751=CARTESIAN_POINT('',(-3.225,2.5,1.));
#9752=CARTESIAN_POINT('Origin',(-3.,2.5,1.));
#9753=CARTESIAN_POINT('',(-3.225,2.5,1.8));
#9754=CARTESIAN_POINT('',(-3.225,2.5,0.9));
#9755=CARTESIAN_POINT('Origin',(-3.,2.5,1.8));
#9756=CARTESIAN_POINT('Origin',(3.,2.5,0.9));
#9757=CARTESIAN_POINT('',(2.775,2.5,1.));
#9758=CARTESIAN_POINT('Origin',(3.,2.5,1.));
#9759=CARTESIAN_POINT('',(2.775,2.5,1.8));
#9760=CARTESIAN_POINT('',(2.775,2.5,0.9));
#9761=CARTESIAN_POINT('Origin',(3.,2.5,1.8));
#9762=CARTESIAN_POINT('Origin',(-1.4142135623731,1.6,2.58578643762691));
#9763=CARTESIAN_POINT('',(-1.5792135623731,1.7,2.58578643762691));
#9764=CARTESIAN_POINT('Origin',(-1.4142135623731,1.7,2.58578643762691));
#9765=CARTESIAN_POINT('',(-1.5792135623731,3.3,2.58578643762691));
#9766=CARTESIAN_POINT('',(-1.5792135623731,1.6,2.58578643762691));
#9767=CARTESIAN_POINT('Origin',(-1.4142135623731,3.3,2.58578643762691));
#9768=CARTESIAN_POINT('Origin',(-1.41421356237309,1.6,5.41421356237309));
#9769=CARTESIAN_POINT('',(-1.57921356237309,1.7,5.41421356237309));
#9770=CARTESIAN_POINT('Origin',(-1.41421356237309,1.7,5.41421356237309));
#9771=CARTESIAN_POINT('',(-1.57921356237309,3.3,5.41421356237309));
#9772=CARTESIAN_POINT('',(-1.57921356237309,1.6,5.41421356237309));
#9773=CARTESIAN_POINT('Origin',(-1.41421356237309,3.3,5.41421356237309));
#9774=CARTESIAN_POINT('Origin',(1.4142135623731,1.6,5.41421356237309));
#9775=CARTESIAN_POINT('',(1.2492135623731,1.7,5.41421356237309));
#9776=CARTESIAN_POINT('Origin',(1.4142135623731,1.7,5.41421356237309));
#9777=CARTESIAN_POINT('',(1.2492135623731,3.3,5.41421356237309));
#9778=CARTESIAN_POINT('',(1.2492135623731,1.6,5.41421356237309));
#9779=CARTESIAN_POINT('Origin',(1.4142135623731,3.3,5.41421356237309));
#9780=CARTESIAN_POINT('Origin',(1.41421356237309,1.6,2.5857864376269));
#9781=CARTESIAN_POINT('',(1.24921356237309,1.7,2.5857864376269));
#9782=CARTESIAN_POINT('Origin',(1.41421356237309,1.7,2.5857864376269));
#9783=CARTESIAN_POINT('',(1.24921356237309,3.3,2.5857864376269));
#9784=CARTESIAN_POINT('',(1.24921356237309,1.6,2.5857864376269));
#9785=CARTESIAN_POINT('Origin',(1.41421356237309,3.3,2.5857864376269));
#9786=CARTESIAN_POINT('Origin',(0.,1.6,4.));
#9787=CARTESIAN_POINT('',(-1.6,1.7,4.));
#9788=CARTESIAN_POINT('Origin',(0.,1.7,4.));
#9789=CARTESIAN_POINT('',(-1.6,3.3,4.));
#9790=CARTESIAN_POINT('',(-1.6,1.6,4.));
#9791=CARTESIAN_POINT('Origin',(0.,3.3,4.));
#9792=CARTESIAN_POINT('Origin',(-3.6,1.7,1.8));
#9793=CARTESIAN_POINT('',(2.4,1.7,1.8));
#9794=CARTESIAN_POINT('',(2.4,3.3,1.8));
#9795=CARTESIAN_POINT('',(2.4,1.7,1.8));
#9796=CARTESIAN_POINT('',(3.6,1.7,1.8));
#9797=CARTESIAN_POINT('',(3.6,1.7,1.8));
#9798=CARTESIAN_POINT('',(3.6,3.3,1.8));
#9799=CARTESIAN_POINT('',(3.6,1.7,1.8));
#9800=CARTESIAN_POINT('',(3.6,3.3,1.8));
#9801=CARTESIAN_POINT('Origin',(-3.6,1.7,1.8));
#9802=CARTESIAN_POINT('',(-2.4,3.3,1.8));
#9803=CARTESIAN_POINT('',(-2.4,1.7,1.8));
#9804=CARTESIAN_POINT('',(-2.4,2.5,1.8));
#9805=CARTESIAN_POINT('',(-3.6,3.3,1.8));
#9806=CARTESIAN_POINT('',(3.6,3.3,1.8));
#9807=CARTESIAN_POINT('',(-3.6,1.7,1.8));
#9808=CARTESIAN_POINT('',(-3.6,1.7,1.8));
#9809=CARTESIAN_POINT('',(3.6,1.7,1.8));
#9810=CARTESIAN_POINT('Origin',(-3.6,1.7,1.));
#9811=CARTESIAN_POINT('',(-3.6,1.7,1.));
#9812=CARTESIAN_POINT('',(-3.6,1.7,1.8));
#9813=CARTESIAN_POINT('',(-3.6,3.3,1.));
#9814=CARTESIAN_POINT('',(-3.6,3.3,1.8));
#9815=CARTESIAN_POINT('',(-3.6,1.7,1.));
#9816=CARTESIAN_POINT('Origin',(3.6,1.7,1.8));
#9817=CARTESIAN_POINT('',(3.6,1.7,1.));
#9818=CARTESIAN_POINT('',(3.6,1.7,1.));
#9819=CARTESIAN_POINT('',(3.6,3.3,1.));
#9820=CARTESIAN_POINT('',(3.6,1.7,1.));
#9821=CARTESIAN_POINT('',(3.6,3.3,1.));
#9822=CARTESIAN_POINT('Origin',(-2.4,1.7,1.));
#9823=CARTESIAN_POINT('',(2.4,1.7,6.5));
#9824=CARTESIAN_POINT('',(2.4,1.7,1.));
#9825=CARTESIAN_POINT('',(-2.4,1.7,6.5));
#9826=CARTESIAN_POINT('',(-2.4,1.7,6.5));
#9827=CARTESIAN_POINT('',(-2.4,1.7,1.));
#9828=CARTESIAN_POINT('',(-3.6,1.7,1.));
#9829=CARTESIAN_POINT('Origin',(2.4,1.7,1.));
#9830=CARTESIAN_POINT('',(2.4,3.3,6.5));
#9831=CARTESIAN_POINT('',(2.4,3.3,1.));
#9832=CARTESIAN_POINT('',(2.4,1.7,6.5));
#9833=CARTESIAN_POINT('Origin',(2.4,3.3,1.));
#9834=CARTESIAN_POINT('',(-2.4,3.3,6.5));
#9835=CARTESIAN_POINT('',(-2.4,3.3,1.));
#9836=CARTESIAN_POINT('',(2.4,3.3,6.5));
#9837=CARTESIAN_POINT('',(-3.6,3.3,1.));
#9838=CARTESIAN_POINT('Origin',(-2.4,3.3,1.));
#9839=CARTESIAN_POINT('',(-2.4,3.3,6.5));
#9840=CARTESIAN_POINT('Origin',(0.,2.5,6.5));
#9841=CARTESIAN_POINT('Origin',(0.,2.5,1.));
#12819=UNCERTAINTY_MEASURE_WITH_UNIT(LENGTH_MEASURE(0.001),#12897,
'DISTANCE_ACCURACY_VALUE',
'Maximum model space distance between geometric entities at asserted c
onnectivities');
#12853=UNCERTAINTY_MEASURE_WITH_UNIT(LENGTH_MEASURE(0.001),#12897,
'DISTANCE_ACCURACY_VALUE',
'Maximum model space distance between geometric entities at asserted c
onnectivities');
#12862=(
GEOMETRIC_REPRESENTATION_CONTEXT(3)
GLOBAL_UNCERTAINTY_ASSIGNED_CONTEXT((#12819))
GLOBAL_UNIT_ASSIGNED_CONTEXT((#12897,#12899,#12900))
REPRESENTATION_CONTEXT('','3D')
);
#12896=(
GEOMETRIC_REPRESENTATION_CONTEXT(3)
GLOBAL_UNCERTAINTY_ASSIGNED_CONTEXT((#12853))
GLOBAL_UNIT_ASSIGNED_CONTEXT((#12897,#12899,#12900))
REPRESENTATION_CONTEXT('','3D')
);
#12897=(
LENGTH_UNIT()
NAMED_UNIT(*)
SI_UNIT(.CENTI.,.METRE.)
);
#12899=(
NAMED_UNIT(*)
PLANE_ANGLE_UNIT()
SI_UNIT($,.RADIAN.)
);
#12900=(
NAMED_UNIT(*)
SI_UNIT($,.STERADIAN.)
SOLID_ANGLE_UNIT()
);
#12909=SHAPE_DEFINITION_REPRESENTATION(#12951,#13062);
#12951=PRODUCT_DEFINITION_SHAPE('',$,#13105);
#13062=SHAPE_REPRESENTATION('',(#6750),#12862);
#13096=PRODUCT_DEFINITION_CONTEXT('part definition',#13224,'design');
#13105=PRODUCT_DEFINITION('Camshaft bearing post (1)',
'Camshaft bearing post (1)',#13147,#13096);
#13147=PRODUCT_DEFINITION_FORMATION('',$,#13234);
#13224=APPLICATION_CONTEXT(
'Core Data for Automotive Mechanical Design Process');
#13225=PRODUCT_CONTEXT('part definition',#13224,'mechanical');
#13234=PRODUCT('Camshaft bearing post (1)','Camshaft bearing post (1)',
'Camshaft bearing post (1)',(#13225));
#13324=COLOUR_RGB('Grey',0.48,0.52,0.57);
#13325=FILL_AREA_STYLE_COLOUR('',#13324);
#13326=FILL_AREA_STYLE('',(#13325));
#13327=SURFACE_STYLE_FILL_AREA(#13326);
#13328=SURFACE_SIDE_STYLE('',(#13327));
#13329=SURFACE_STYLE_USAGE(.BOTH.,#13328);
#13330=PRESENTATION_STYLE_ASSIGNMENT((#13329));
ENDSEC;
END-ISO-10303-21;
